ISO-10303-21;
HEADER;
FILE_DESCRIPTION (('STEP AP214'),
    '1' );
FILE_NAME ('socket head cap screw_iso_ISO 4762 M6 x 20 - 20N.step',
    '2026-10-20T14:49:59',
    ( '' ),
    ( '' ),
    'SwSTEP 2.0',
    'SolidWorks 2025',
    '' );
FILE_SCHEMA (( 'AUTOMOTIVE_DESIGN' ));
ENDSEC;

DATA;
#2=CARTESIAN_POINT ( 'NONE',  ( 3.000000000000000000, 2.935248768560057897, -3.252606517456513302E-15 ) ) ;
#27=ORIENTED_EDGE ( 'NONE', *, *, #3979, .T. ) ;
#29=CARTESIAN_POINT ( 'NONE',  ( 3.000000000000000000, 0.000000000000000000, 0.000000000000000000 ) ) ;
#32=EDGE_CURVE ( 'NONE', #6206, #5311, #7708, .T. ) ;
#77=DIRECTION ( 'NONE',  ( -1.000000000000000000, 0.000000000000000000, 0.000000000000000000 ) ) ;
#78=DIRECTION ( 'NONE',  ( 0.000000000000000000, 1.000000000000000000, -1.329743448921560837E-15 ) ) ;
#88=ORIENTED_EDGE ( 'NONE', *, *, #32, .T. ) ;
#90=ADVANCED_FACE ( 'NONE', ( #4832 ), #5200, .F. ) ;
#94=FACE_OUTER_BOUND ( 'NONE', #233, .T. ) ;
#105=EDGE_CURVE ( 'NONE', #8005, #7120, #1404, .T. ) ;
#106=DIRECTION ( 'NONE',  ( -1.000000000000000000, -0.000000000000000000, -0.000000000000000000 ) ) ;
#107=DIRECTION ( 'NONE',  ( 0.000000000000000000, 0.000000000000000000, 1.000000000000000000 ) ) ;
#146=AXIS2_PLACEMENT_3D ( 'NONE', #654, #6367, #4769 ) ;
#182=PRODUCT_DEFINITION_CONTEXT ( 'detailed design', #6258, 'design' ) ;
#212=ADVANCED_FACE ( 'NONE', ( #4987 ), #7922, .T. ) ;
#214=AXIS2_PLACEMENT_3D ( 'NONE', #6935, #10169, #2741 ) ;
#233=EDGE_LOOP ( 'NONE', ( #9990, #9923, #6076 ) ) ;
#278=DIRECTION ( 'NONE',  ( 0.000000000000000000, 0.000000000000000000, 1.000000000000000000 ) ) ;
#328=ORIENTED_EDGE ( 'NONE', *, *, #6700, .F. ) ;
#345=ADVANCED_FACE ( 'NONE', ( #9025 ), #8120, .T. ) ;
#363=EDGE_LOOP ( 'NONE', ( #8107, #2438, #3383, #9676 ) ) ;
#364=DIRECTION ( 'NONE',  ( 0.000000000000000000, 0.8660254037844379305, -0.5000000000000012212 ) ) ;
#379=( GEOMETRIC_REPRESENTATION_CONTEXT ( 3 ) GLOBAL_UNCERTAINTY_ASSIGNED_CONTEXT ( ( #4097 ) ) GLOBAL_UNIT_ASSIGNED_CONTEXT ( ( #7158, #2376, #5505 ) ) REPRESENTATION_CONTEXT ( 'NONE', 'WORKASPACE' ) );
#384=DIRECTION ( 'NONE',  ( -1.000000000000000000, -0.000000000000000000, -0.000000000000000000 ) ) ;
#395=CIRCLE ( 'NONE', #5122, 2.541999999999999815 ) ;
#411=( LENGTH_UNIT ( ) NAMED_UNIT ( * ) SI_UNIT ( .MILLI., .METRE. ) );
#417=EDGE_LOOP ( 'NONE', ( #9129, #8293, #8027, #4721 ) ) ;
#422=DIRECTION ( 'NONE',  ( -1.000000000000000000, -0.000000000000000000, -0.000000000000000000 ) ) ;
#428=EDGE_CURVE ( 'NONE', #3827, #4373, #811, .T. ) ;
#468=ORIENTED_EDGE ( 'NONE', *, *, #2360, .F. ) ;
#472=CARTESIAN_POINT ( 'NONE',  ( 3.000000000000000000, 0.000000000000000000, 0.000000000000000000 ) ) ;
#477=VERTEX_POINT ( 'NONE', #4411 ) ;
#519=CARTESIAN_POINT ( 'NONE',  ( 0.000000000000000000, -1.467624384280024730, 2.542000000000003368 ) ) ;
#543=DIRECTION ( 'NONE',  ( 0.000000000000000000, 0.000000000000000000, -1.000000000000000000 ) ) ;
#558=ADVANCED_FACE ( 'NONE', ( #9507 ), #6568, .T. ) ;
#565=EDGE_LOOP ( 'NONE', ( #3764, #4781, #1122, #8407, #4538 ) ) ;
#572=DIRECTION ( 'NONE',  ( -1.000000000000000000, 0.000000000000000000, 0.000000000000000000 ) ) ;
#588=CARTESIAN_POINT ( 'NONE',  ( 26.00000000000000355, 0.000000000000000000, 2.445500000000000007 ) ) ;
#600=CARTESIAN_POINT ( 'NONE',  ( 26.00000000000000355, 0.000000000000000000, 0.000000000000000000 ) ) ;
#622=ORIENTED_EDGE ( 'NONE', *, *, #3207, .F. ) ;
#624=DIRECTION ( 'NONE',  ( 0.000000000000000000, 0.000000000000000000, 1.000000000000000000 ) ) ;
#647=FACE_OUTER_BOUND ( 'NONE', #2117, .T. ) ;
#654=CARTESIAN_POINT ( 'NONE',  ( 0.3000000000000016542, 0.000000000000000000, 0.000000000000000000 ) ) ;
#673=CIRCLE ( 'NONE', #7114, 0.2999999999999999334 ) ;
#678=EDGE_CURVE ( 'NONE', #9023, #6043, #1805, .T. ) ;
#679=CYLINDRICAL_SURFACE ( 'NONE', #6216, 5.000000000000000000 ) ;
#711=AXIS2_PLACEMENT_3D ( 'NONE', #4492, #7625, #2051 ) ;
#759=CIRCLE ( 'NONE', #7197, 2.541999999999999815 ) ;
#783=VECTOR ( 'NONE', #2800, 999.9999999999998863 ) ;
#788=LINE ( 'NONE', #2, #1240 ) ;
#792=ORIENTED_EDGE ( 'NONE', *, *, #6700, .T. ) ;
#811=CIRCLE ( 'NONE', #10126, 3.250000000000000444 ) ;
#828=FACE_OUTER_BOUND ( 'NONE', #5278, .T. ) ;
#853=LINE ( 'NONE', #4144, #7394 ) ;
#910=VERTEX_POINT ( 'NONE', #2118 ) ;
#940=DIRECTION ( 'NONE',  ( 0.000000000000000000, 0.000000000000000000, 1.000000000000000000 ) ) ;
#958=AXIS2_PLACEMENT_3D ( 'NONE', #8255, #9913, #940 ) ;
#987=DIRECTION ( 'NONE',  ( 0.000000000000000000, 0.000000000000000000, 1.000000000000000000 ) ) ;
#1022=DIRECTION ( 'NONE',  ( -0.7071067811865431318, 8.659560562354989558E-17, -0.7071067811865520136 ) ) ;
#1023=LINE ( 'NONE', #9891, #1119 ) ;
#1028=VERTEX_POINT ( 'NONE', #6354 ) ;
#1050=CARTESIAN_POINT ( 'NONE',  ( 3.000000000000000000, -1.467624384280024730, 2.542000000000003368 ) ) ;
#1057=VERTEX_POINT ( 'NONE', #7843 ) ;
#1061=FACE_OUTER_BOUND ( 'NONE', #2659, .T. ) ;
#1066=EDGE_CURVE ( 'NONE', #9437, #7226, #4661, .T. ) ;
#1072=CARTESIAN_POINT ( 'NONE',  ( 3.000000000000000000, -1.467624384280024730, 2.542000000000003368 ) ) ;
#1076=CARTESIAN_POINT ( 'NONE',  ( 3.000000000000000000, -1.467624384280024730, 2.542000000000003368 ) ) ;
#1082=AXIS2_PLACEMENT_3D ( 'NONE', #1833, #6441, #9144 ) ;
#1085=DIRECTION ( 'NONE',  ( 0.000000000000000000, 0.000000000000000000, 1.000000000000000000 ) ) ;
#1099=CIRCLE ( 'NONE', #4798, 5.000000000000000000 ) ;
#1119=VECTOR ( 'NONE', #7385, 1000.000000000000000 ) ;
#1122=ORIENTED_EDGE ( 'NONE', *, *, #7750, .F. ) ;
#1135=DIRECTION ( 'NONE',  ( 0.000000000000000000, 0.000000000000000000, 1.000000000000000000 ) ) ;
#1144=CARTESIAN_POINT ( 'NONE',  ( 26.00000000000000355, 0.000000000000000000, 0.000000000000000000 ) ) ;
#1147=VECTOR ( 'NONE', #9282, 999.9999999999998863 ) ;
#1203=CARTESIAN_POINT ( 'NONE',  ( 3.000000000000000000, 2.935248768560057897, -3.252606517456513302E-15 ) ) ;
#1229=AXIS2_PLACEMENT_3D ( 'NONE', #2526, #8196, #9147 ) ;
#1238=CARTESIAN_POINT ( 'NONE',  ( 6.250000000000005329, 3.673940397442060361E-16, -3.000000000000000444 ) ) ;
#1240=VECTOR ( 'NONE', #5404, 1000.000000000000000 ) ;
#1244=DIRECTION ( 'NONE',  ( -1.000000000000000000, 0.000000000000000000, 0.000000000000000000 ) ) ;
#1278=AXIS2_PLACEMENT_3D ( 'NONE', #5647, #4167, #987 ) ;
#1300=VECTOR ( 'NONE', #2207, 1000.000000000000114 ) ;
#1313=CARTESIAN_POINT ( 'NONE',  ( 0.000000000000000000, 1.467624384280025174, -2.542000000000001592 ) ) ;
#1317=DIRECTION ( 'NONE',  ( -1.000000000000000000, -0.000000000000000000, -0.000000000000000000 ) ) ;
#1328=VECTOR ( 'NONE', #3333, 1000.000000000000000 ) ;
#1364=EDGE_LOOP ( 'NONE', ( #8851, #10286, #468 ) ) ;
#1390=ORIENTED_EDGE ( 'NONE', *, *, #7674, .F. ) ;
#1397=ADVANCED_FACE ( 'NONE', ( #10012 ), #3914, .T. ) ;
#1404=LINE ( 'NONE', #8769, #9445 ) ;
#1406=VECTOR ( 'NONE', #3370, 1000.000000000000000 ) ;
#1413=VECTOR ( 'NONE', #6522, 1000.000000000000000 ) ;
#1430=DIRECTION ( 'NONE',  ( 0.000000000000000000, 1.000000000000000000, -1.329743448921560837E-15 ) ) ;
#1440=EDGE_CURVE ( 'NONE', #9059, #10117, #7146, .T. ) ;
#1480=VECTOR ( 'NONE', #8113, 1000.000000000000000 ) ;
#1484=PLANE ( 'NONE',  #7384 ) ;
#1498=EDGE_LOOP ( 'NONE', ( #3886, #8646, #4986, #9342 ) ) ;
#1507=ORIENTED_EDGE ( 'NONE', *, *, #3207, .T. ) ;
#1517=CARTESIAN_POINT ( 'NONE',  ( -31.74999999999995737, 0.000000000000000000, 0.000000000000000000 ) ) ;
#1542=EDGE_CURVE ( 'NONE', #2621, #910, #1023, .T. ) ;
#1545=ORIENTED_EDGE ( 'NONE', *, *, #6642, .F. ) ;
#1600=ORIENTED_EDGE ( 'NONE', *, *, #4252, .F. ) ;
#1613=VERTEX_POINT ( 'NONE', #5839 ) ;
#1650=CLOSED_SHELL ( 'NONE', ( #7791, #3659, #9210, #212, #5565, #7031, #9427, #3445, #2066, #4946, #1859, #4633, #90, #558, #8713, #9425, #9166, #8376, #7968, #2461, #345, #3557, #7629, #1397, #2302, #4694, #4269 ) ) ;
#1652=AXIS2_PLACEMENT_3D ( 'NONE', #1809, #7430, #9122 ) ;
#1672=ORIENTED_EDGE ( 'NONE', *, *, #105, .F. ) ;
#1677=LINE ( 'NONE', #4849, #5306 ) ;
#1693=EDGE_LOOP ( 'NONE', ( #5685, #1938, #1873 ) ) ;
#1718=ORIENTED_EDGE ( 'NONE', *, *, #9977, .F. ) ;
#1768=DIRECTION ( 'NONE',  ( 0.000000000000000000, 0.000000000000000000, -1.000000000000000000 ) ) ;
#1791=ORIENTED_EDGE ( 'NONE', *, *, #4447, .F. ) ;
#1798=PLANE ( 'NONE',  #3297 ) ;
#1805=LINE ( 'NONE', #9013, #4531 ) ;
#1809=CARTESIAN_POINT ( 'NONE',  ( 6.250000000000005329, 0.000000000000000000, -3.250000000000000444 ) ) ;
#1820=CARTESIAN_POINT ( 'NONE',  ( 3.000000000000000000, -1.467624384280032279, -2.541999999999998039 ) ) ;
#1824=ORIENTED_EDGE ( 'NONE', *, *, #2233, .T. ) ;
#1833=CARTESIAN_POINT ( 'NONE',  ( 3.000000000000000000, 2.935248768560057897, -3.252606517456513302E-15 ) ) ;
#1850=CARTESIAN_POINT ( 'NONE',  ( 3.000000000000000000, -1.467624384280024730, 2.542000000000003368 ) ) ;
#1859=ADVANCED_FACE ( 'NONE', ( #2242 ), #4679, .T. ) ;
#1864=EDGE_LOOP ( 'NONE', ( #4693, #2674, #4241, #1507, #2287, #1672 ) ) ;
#1865=CARTESIAN_POINT ( 'NONE',  ( 3.000000000000000000, 0.000000000000000000, 0.000000000000000000 ) ) ;
#1866=ORIENTED_EDGE ( 'NONE', *, *, #5218, .F. ) ;
#1873=ORIENTED_EDGE ( 'NONE', *, *, #1973, .T. ) ;
#1877=CIRCLE ( 'NONE', #6619, 3.250000000000000444 ) ;
#1885=CARTESIAN_POINT ( 'NONE',  ( 0.000000000000000000, -1.467624384280024730, 2.542000000000003368 ) ) ;
#1895=DIRECTION ( 'NONE',  ( -0.000000000000000000, 0.8660254037844394848, 0.4999999999999985567 ) ) ;
#1922=VECTOR ( 'NONE', #3126, 1000.000000000000000 ) ;
#1924=DIRECTION ( 'NONE',  ( -1.000000000000000000, -0.000000000000000000, -0.000000000000000000 ) ) ;
#1938=ORIENTED_EDGE ( 'NONE', *, *, #1440, .F. ) ;
#1940=ORIENTED_EDGE ( 'NONE', *, *, #6325, .T. ) ;
#1960=LINE ( 'NONE', #5350, #1147 ) ;
#1966=CIRCLE ( 'NONE', #5002, 3.000000000000000444 ) ;
#1973=EDGE_CURVE ( 'NONE', #9059, #5268, #7684, .T. ) ;
#2032=EDGE_CURVE ( 'NONE', #7226, #9088, #2221, .T. ) ;
#2051=DIRECTION ( 'NONE',  ( 0.000000000000000000, 0.000000000000000000, 1.000000000000000000 ) ) ;
#2066=ADVANCED_FACE ( 'NONE', ( #8838, #3273 ), #1484, .T. ) ;
#2090=CIRCLE ( 'NONE', #6156, 5.000000000000000000 ) ;
#2096=SHAPE_REPRESENTATION_RELATIONSHIP ( 'NONE' , 'NONE' ,  #5068, #6825 ) ;
#2117=EDGE_LOOP ( 'NONE', ( #4126, #8092, #5054, #10088 ) ) ;
#2118=CARTESIAN_POINT ( 'NONE',  ( 6.250000000000005329, 0.000000000000000000, 3.000000000000000444 ) ) ;
#2133=VECTOR ( 'NONE', #3807, 1000.000000000000114 ) ;
#2140=ORIENTED_EDGE ( 'NONE', *, *, #9977, .T. ) ;
#2207=DIRECTION ( 'NONE',  ( 0.000000000000000000, -0.5000000000000011102, -0.8660254037844379305 ) ) ;
#2210=CARTESIAN_POINT ( 'NONE',  ( 3.000000000000000000, 1.467624384280032501, 2.541999999999999371 ) ) ;
#2215=FACE_OUTER_BOUND ( 'NONE', #4543, .T. ) ;
#2221=LINE ( 'NONE', #6140, #3154 ) ;
#2233=EDGE_CURVE ( 'NONE', #5001, #8168, #7460, .T. ) ;
#2239=ORIENTED_EDGE ( 'NONE', *, *, #5458, .F. ) ;
#2242=FACE_OUTER_BOUND ( 'NONE', #417, .T. ) ;
#2243=DIRECTION ( 'NONE',  ( 0.000000000000000000, 0.000000000000000000, 1.000000000000000000 ) ) ;
#2248=ORIENTED_EDGE ( 'NONE', *, *, #7081, .T. ) ;
#2253=VECTOR ( 'NONE', #8388, 1000.000000000000000 ) ;
#2255=LINE ( 'NONE', #5375, #5826 ) ;
#2256=DIRECTION ( 'NONE',  ( -1.000000000000000000, -0.000000000000000000, -0.000000000000000000 ) ) ;
#2277=CARTESIAN_POINT ( 'NONE',  ( 6.000000000000005329, 5.000000000000000000, 0.000000000000000000 ) ) ;
#2287=ORIENTED_EDGE ( 'NONE', *, *, #7815, .F. ) ;
#2302=ADVANCED_FACE ( 'NONE', ( #9968 ), #6560, .T. ) ;
#2308=VECTOR ( 'NONE', #4326, 1000.000000000000114 ) ;
#2325=AXIS2_PLACEMENT_3D ( 'NONE', #9623, #9776, #5624 ) ;
#2347=FACE_OUTER_BOUND ( 'NONE', #9830, .T. ) ;
#2354=DIRECTION ( 'NONE',  ( 0.000000000000000000, 0.000000000000000000, -1.000000000000000000 ) ) ;
#2360=EDGE_CURVE ( 'NONE', #1028, #5001, #6233, .T. ) ;
#2368=DIRECTION ( 'NONE',  ( 0.000000000000000000, 0.000000000000000000, -1.000000000000000000 ) ) ;
#2376=( NAMED_UNIT ( * ) PLANE_ANGLE_UNIT ( ) SI_UNIT ( $, .RADIAN. ) );
#2377=CARTESIAN_POINT ( 'NONE',  ( 0.000000000000000000, 2.935248768560057897, -3.252606517456513302E-15 ) ) ;
#2390=PLANE ( 'NONE',  #10373 ) ;
#2423=DIRECTION ( 'NONE',  ( 0.000000000000000000, 0.000000000000000000, -1.000000000000000000 ) ) ;
#2433=CARTESIAN_POINT ( 'NONE',  ( 3.000000000000000000, 0.000000000000000000, 0.000000000000000000 ) ) ;
#2438=ORIENTED_EDGE ( 'NONE', *, *, #5905, .T. ) ;
#2461=ADVANCED_FACE ( 'NONE', ( #4390 ), #7622, .F. ) ;
#2482=DIRECTION ( 'NONE',  ( -0.000000000000000000, 1.329743448921560837E-15, 1.000000000000000000 ) ) ;
#2495=CARTESIAN_POINT ( 'NONE',  ( 0.000000000000000000, 1.467624384280025174, -2.542000000000001592 ) ) ;
#2498=VERTEX_POINT ( 'NONE', #7141 ) ;
#2499=CYLINDRICAL_SURFACE ( 'NONE', #5532, 3.000000000000000444 ) ;
#2526=CARTESIAN_POINT ( 'NONE',  ( 5.999999999999998224, 0.000000000000000000, 0.000000000000000000 ) ) ;
#2545=ORIENTED_EDGE ( 'NONE', *, *, #4863, .T. ) ;
#2589=CONICAL_SURFACE ( 'NONE', #6826, 2.541999999999999815, 1.047197551196591858 ) ;
#2621=VERTEX_POINT ( 'NONE', #4059 ) ;
#2633=DIRECTION ( 'NONE',  ( 1.000000000000000000, 0.000000000000000000, 0.000000000000000000 ) ) ;
#2659=EDGE_LOOP ( 'NONE', ( #4320, #7425, #4589, #2248, #9197 ) ) ;
#2668=PLANE ( 'NONE',  #8879 ) ;
#2670=CARTESIAN_POINT ( 'NONE',  ( 3.000000000000000000, 2.201436576420041202, -1.271000000000003016 ) ) ;
#2674=ORIENTED_EDGE ( 'NONE', *, *, #2032, .F. ) ;
#2709=VERTEX_POINT ( 'NONE', #9040 ) ;
#2726=DIRECTION ( 'NONE',  ( -1.000000000000000000, -0.000000000000000000, -0.000000000000000000 ) ) ;
#2739=VERTEX_POINT ( 'NONE', #3420 ) ;
#2741=DIRECTION ( 'NONE',  ( 0.000000000000000000, 0.000000000000000000, 1.000000000000000000 ) ) ;
#2751=EDGE_CURVE ( 'NONE', #5926, #4123, #5899, .T. ) ;
#2797=CIRCLE ( 'NONE', #4157, 3.000000000000000444 ) ;
#2800=DIRECTION ( 'NONE',  ( 0.000000000000000000, -0.5000000000000012212, -0.8660254037844380415 ) ) ;
#2835=DIRECTION ( 'NONE',  ( 0.000000000000000000, 0.000000000000000000, 1.000000000000000000 ) ) ;
#2848=CYLINDRICAL_SURFACE ( 'NONE', #711, 5.000000000000000000 ) ;
#2926=CARTESIAN_POINT ( 'NONE',  ( 3.000000000000000000, 2.201436576420045199, 1.270999999999996355 ) ) ;
#2936=DIRECTION ( 'NONE',  ( -1.000000000000000000, -0.000000000000000000, -0.000000000000000000 ) ) ;
#2941=ORIENTED_EDGE ( 'NONE', *, *, #6494, .T. ) ;
#2967=ORIENTED_EDGE ( 'NONE', *, *, #1066, .F. ) ;
#3042=EDGE_CURVE ( 'NONE', #9023, #10117, #9127, .T. ) ;
#3060=DIRECTION ( 'NONE',  ( -0.5000000000000051070, 1.060575238724903217E-16, -0.8660254037844355990 ) ) ;
#3068=VERTEX_POINT ( 'NONE', #6740 ) ;
#3081=EDGE_CURVE ( 'NONE', #8380, #4123, #673, .T. ) ;
#3112=DIRECTION ( 'NONE',  ( 1.000000000000000000, 0.000000000000000000, 0.000000000000000000 ) ) ;
#3113=( GEOMETRIC_REPRESENTATION_CONTEXT ( 3 ) GLOBAL_UNCERTAINTY_ASSIGNED_CONTEXT ( ( #9938 ) ) GLOBAL_UNIT_ASSIGNED_CONTEXT ( ( #411, #7718, #4387 ) ) REPRESENTATION_CONTEXT ( 'NONE', 'WORKASPACE' ) );
#3123=ORIENTED_EDGE ( 'NONE', *, *, #6366, .F. ) ;
#3126=DIRECTION ( 'NONE',  ( -1.000000000000000000, -0.000000000000000000, -0.000000000000000000 ) ) ;
#3132=AXIS2_PLACEMENT_3D ( 'NONE', #10347, #7161, #7905 ) ;
#3137=FACE_OUTER_BOUND ( 'NONE', #9843, .T. ) ;
#3154=VECTOR ( 'NONE', #1430, 1000.000000000000000 ) ;
#3177=CARTESIAN_POINT ( 'NONE',  ( 0.000000000000000000, 5.939536975864662969E-16, -4.700000000000000178 ) ) ;
#3182=EDGE_CURVE ( 'NONE', #4123, #5926, #5236, .T. ) ;
#3189=DIRECTION ( 'NONE',  ( 0.000000000000000000, -0.5000000000000011102, -0.8660254037844379305 ) ) ;
#3207=EDGE_CURVE ( 'NONE', #8168, #8465, #3386, .T. ) ;
#3238=ORIENTED_EDGE ( 'NONE', *, *, #8687, .T. ) ;
#3273=FACE_OUTER_BOUND ( 'NONE', #4143, .T. ) ;
#3291=LINE ( 'NONE', #9929, #4775 ) ;
#3297=AXIS2_PLACEMENT_3D ( 'NONE', #1850, #2482, #9920 ) ;
#3301=DIRECTION ( 'NONE',  ( 0.000000000000000000, 0.000000000000000000, 1.000000000000000000 ) ) ;
#3302=CARTESIAN_POINT ( 'NONE',  ( 26.00000000000000355, 2.994873747314852478E-16, -2.445500000000000007 ) ) ;
#3313=EDGE_CURVE ( 'NONE', #1057, #7120, #9322, .T. ) ;
#3333=DIRECTION ( 'NONE',  ( -1.000000000000000000, -0.000000000000000000, -0.000000000000000000 ) ) ;
#3344=ORIENTED_EDGE ( 'NONE', *, *, #2751, .T. ) ;
#3351=AXIS2_PLACEMENT_3D ( 'NONE', #6743, #7438, #8334 ) ;
#3370=DIRECTION ( 'NONE',  ( 0.000000000000000000, -1.000000000000000000, 1.329743448921561232E-15 ) ) ;
#3376=DIRECTION ( 'NONE',  ( 0.000000000000000000, -0.4999999999999985567, 0.8660254037844394848 ) ) ;
#3377=PLANE ( 'NONE',  #1278 ) ;
#3383=ORIENTED_EDGE ( 'NONE', *, *, #4237, .T. ) ;
#3386=LINE ( 'NONE', #5816, #6414 ) ;
#3387=CARTESIAN_POINT ( 'NONE',  ( 0.000000000000000000, -2.935248768560057009, 4.770489558936219510E-15 ) ) ;
#3405=ORIENTED_EDGE ( 'NONE', *, *, #10002, .T. ) ;
#3420=CARTESIAN_POINT ( 'NONE',  ( 5.999999999999998224, 6.123233995736766282E-16, -5.000000000000000000 ) ) ;
#3421=ORIENTED_EDGE ( 'NONE', *, *, #4237, .F. ) ;
#3424=DIRECTION ( 'NONE',  ( 0.000000000000000000, 0.000000000000000000, 1.000000000000000000 ) ) ;
#3445=ADVANCED_FACE ( 'NONE', ( #3963 ), #679, .T. ) ;
#3450=ORIENTED_EDGE ( 'NONE', *, *, #7348, .T. ) ;
#3476=CARTESIAN_POINT ( 'NONE',  ( 3.000000000000000000, 1.467624384280032501, 2.541999999999999371 ) ) ;
#3484=CARTESIAN_POINT ( 'NONE',  ( 3.000000000000000000, -2.935248768560057009, 4.770489558936219510E-15 ) ) ;
#3495=EDGE_LOOP ( 'NONE', ( #10460, #8665, #7061, #4765 ) ) ;
#3512=VECTOR ( 'NONE', #2936, 1000.000000000000000 ) ;
#3552=AXIS2_PLACEMENT_3D ( 'NONE', #1865, #384, #9126 ) ;
#3557=ADVANCED_FACE ( 'NONE', ( #5956 ), #9308, .T. ) ;
#3589=DIRECTION ( 'NONE',  ( 0.000000000000000000, 0.5000000000000012212, 0.8660254037844379305 ) ) ;
#3599=CARTESIAN_POINT ( 'NONE',  ( 0.3000000000000016542, 6.123233995736766282E-16, -5.000000000000000000 ) ) ;
#3632=CARTESIAN_POINT ( 'NONE',  ( -31.74999999999995737, 3.673940397442060361E-16, -3.000000000000000444 ) ) ;
#3659=ADVANCED_FACE ( 'NONE', ( #7557 ), #9257, .T. ) ;
#3686=EDGE_CURVE ( 'NONE', #6043, #9088, #7926, .T. ) ;
#3706=PLANE ( 'NONE',  #9034 ) ;
#3726=ORIENTED_EDGE ( 'NONE', *, *, #5564, .T. ) ;
#3746=CARTESIAN_POINT ( 'NONE',  ( 3.000000000000000000, -1.467624384280024730, 2.542000000000003368 ) ) ;
#3764=ORIENTED_EDGE ( 'NONE', *, *, #7815, .T. ) ;
#3807=DIRECTION ( 'NONE',  ( 0.000000000000000000, -0.4999999999999985567, 0.8660254037844394848 ) ) ;
#3817=CARTESIAN_POINT ( 'NONE',  ( 3.000000000000000000, 2.935248768560057897, -3.252606517456513302E-15 ) ) ;
#3827=VERTEX_POINT ( 'NONE', #9984 ) ;
#3834=DIRECTION ( 'NONE',  ( 0.000000000000000000, 0.000000000000000000, 1.000000000000000000 ) ) ;
#3857=ORIENTED_EDGE ( 'NONE', *, *, #1066, .T. ) ;
#3867=EDGE_CURVE ( 'NONE', #2739, #8380, #5828, .T. ) ;
#3886=ORIENTED_EDGE ( 'NONE', *, *, #5564, .F. ) ;
#3914=PLANE ( 'NONE',  #7214 ) ;
#3930=LINE ( 'NONE', #7160, #1922 ) ;
#3954=CARTESIAN_POINT ( 'NONE',  ( 6.250000000000005329, 3.980102097228898231E-16, 3.250000000000000444 ) ) ;
#3961=EDGE_LOOP ( 'NONE', ( #10348, #2941, #9768, #9086 ) ) ;
#3963=FACE_OUTER_BOUND ( 'NONE', #363, .T. ) ;
#3966=CARTESIAN_POINT ( 'NONE',  ( 3.000000000000000000, -2.201436576420044755, -1.270999999999995911 ) ) ;
#3979=EDGE_CURVE ( 'NONE', #5311, #3827, #8594, .T. ) ;
#3986=AXIS2_PLACEMENT_3D ( 'NONE', #8732, #3112, #2368 ) ;
#3992=EDGE_CURVE ( 'NONE', #5268, #1057, #1960, .T. ) ;
#4027=CARTESIAN_POINT ( 'NONE',  ( 3.000000000000000000, 0.000000000000000000, 2.541999999999999815 ) ) ;
#4049=DIRECTION ( 'NONE',  ( 1.000000000000000000, 0.000000000000000000, 0.000000000000000000 ) ) ;
#4059=CARTESIAN_POINT ( 'NONE',  ( 25.44550000000000978, 0.000000000000000000, 2.999999999999999556 ) ) ;
#4072=DIRECTION ( 'NONE',  ( -0.5000000000000051070, 0.000000000000000000, 0.8660254037844355990 ) ) ;
#4086=VECTOR ( 'NONE', #1022, 999.9999999999998863 ) ;
#4087=LINE ( 'NONE', #5883, #1413 ) ;
#4094=MECHANICAL_DESIGN_GEOMETRIC_PRESENTATION_REPRESENTATION('',(#5770),#379);
#4097=UNCERTAINTY_MEASURE_WITH_UNIT (LENGTH_MEASURE( 1.000000000000000082E-05 ), #7158, 'distance_accuracy_value', 'NONE');
#4123=VERTEX_POINT ( 'NONE', #3177 ) ;
#4126=ORIENTED_EDGE ( 'NONE', *, *, #5142, .F. ) ;
#4132=FACE_BOUND ( 'NONE', #1864, .T. ) ;
#4143=EDGE_LOOP ( 'NONE', ( #1791, #10399 ) ) ;
#4144=CARTESIAN_POINT ( 'NONE',  ( 3.000000000000000000, -1.467624384280024730, 2.542000000000003368 ) ) ;
#4147=AXIS2_PLACEMENT_3D ( 'NONE', #6569, #5132, #7520 ) ;
#4156=CARTESIAN_POINT ( 'NONE',  ( 6.250000000000005329, 0.000000000000000000, 0.000000000000000000 ) ) ;
#4157=AXIS2_PLACEMENT_3D ( 'NONE', #10228, #6082, #5131 ) ;
#4167=DIRECTION ( 'NONE',  ( -1.000000000000000000, 0.000000000000000000, 0.000000000000000000 ) ) ;
#4185=PLANE ( 'NONE',  #4147 ) ;
#4187=ORIENTED_EDGE ( 'NONE', *, *, #8050, .F. ) ;
#4199=ORIENTED_EDGE ( 'NONE', *, *, #2360, .T. ) ;
#4236=ORIENTED_EDGE ( 'NONE', *, *, #4618, .F. ) ;
#4237=EDGE_CURVE ( 'NONE', #10107, #477, #3930, .T. ) ;
#4241=ORIENTED_EDGE ( 'NONE', *, *, #4929, .T. ) ;
#4249=DIRECTION ( 'NONE',  ( 0.000000000000000000, -1.224646799147353207E-16, 1.000000000000000000 ) ) ;
#4252=EDGE_CURVE ( 'NONE', #1613, #9607, #759, .T. ) ;
#4269=ADVANCED_FACE ( 'NONE', ( #9109 ), #4634, .F. ) ;
#4278=ORIENTED_EDGE ( 'NONE', *, *, #1973, .F. ) ;
#4293=CARTESIAN_POINT ( 'NONE',  ( 3.000000000000000000, 0.000000000000000000, 0.000000000000000000 ) ) ;
#4319=CARTESIAN_POINT ( 'NONE',  ( 0.000000000000000000, 0.000000000000000000, 0.000000000000000000 ) ) ;
#4320=ORIENTED_EDGE ( 'NONE', *, *, #6959, .F. ) ;
#4326=DIRECTION ( 'NONE',  ( 0.000000000000000000, -0.5000000000000011102, -0.8660254037844379305 ) ) ;
#4356=CARTESIAN_POINT ( 'NONE',  ( 0.3000000000000016542, 5.755839955992559655E-16, -4.700000000000000178 ) ) ;
#4363=CARTESIAN_POINT ( 'NONE',  ( 5.999999999999998224, 0.000000000000000000, 5.000000000000000000 ) ) ;
#4373=VERTEX_POINT ( 'NONE', #4864 ) ;
#4387=( NAMED_UNIT ( * ) SI_UNIT ( $, .STERADIAN. ) SOLID_ANGLE_UNIT ( ) );
#4390=FACE_OUTER_BOUND ( 'NONE', #6470, .T. ) ;
#4409=ORIENTED_EDGE ( 'NONE', *, *, #428, .T. ) ;
#4411=CARTESIAN_POINT ( 'NONE',  ( 0.3000000000000016542, 0.000000000000000000, 5.000000000000000000 ) ) ;
#4447=EDGE_CURVE ( 'NONE', #10107, #2739, #1099, .T. ) ;
#4492=CARTESIAN_POINT ( 'NONE',  ( -31.74999999999995737, 0.000000000000000000, 0.000000000000000000 ) ) ;
#4495=CARTESIAN_POINT ( 'NONE',  ( 3.000000000000000000, -2.935248768560057009, 4.770489558936219510E-15 ) ) ;
#4508=CIRCLE ( 'NONE', #9418, 2.445500000000000007 ) ;
#4516=EDGE_CURVE ( 'NONE', #5311, #910, #2797, .T. ) ;
#4531=VECTOR ( 'NONE', #9770, 1000.000000000000000 ) ;
#4538=ORIENTED_EDGE ( 'NONE', *, *, #3313, .T. ) ;
#4543=EDGE_LOOP ( 'NONE', ( #9341, #1866 ) ) ;
#4552=AXIS2_PLACEMENT_3D ( 'NONE', #4319, #8189, #1085 ) ;
#4589=ORIENTED_EDGE ( 'NONE', *, *, #4252, .T. ) ;
#4591=CIRCLE ( 'NONE', #8150, 2.999999999999999556 ) ;
#4601=AXIS2_PLACEMENT_3D ( 'NONE', #8586, #5983, #5928 ) ;
#4618=EDGE_CURVE ( 'NONE', #2709, #1613, #10380, .T. ) ;
#4625=LINE ( 'NONE', #9827, #8226 ) ;
#4633=ADVANCED_FACE ( 'NONE', ( #2215 ), #5444, .T. ) ;
#4634=CONICAL_SURFACE ( 'NONE', #8032, 2.541999999999999815, 1.047197551196591858 ) ;
#4661=LINE ( 'NONE', #9809, #1328 ) ;
#4667=ORIENTED_EDGE ( 'NONE', *, *, #9826, .T. ) ;
#4677=DIRECTION ( 'NONE',  ( -1.000000000000000000, -0.000000000000000000, -0.000000000000000000 ) ) ;
#4679=CONICAL_SURFACE ( 'NONE', #5186, 2.445500000000000007, 0.7853981633974547183 ) ;
#4683=DIRECTION ( 'NONE',  ( -1.000000000000000000, -0.000000000000000000, -0.000000000000000000 ) ) ;
#4693=ORIENTED_EDGE ( 'NONE', *, *, #5458, .T. ) ;
#4694=ADVANCED_FACE ( 'NONE', ( #94 ), #3377, .T. ) ;
#4701=AXIS2_PLACEMENT_3D ( 'NONE', #7332, #77, #3301 ) ;
#4718=DIRECTION ( 'NONE',  ( 0.000000000000000000, 1.000000000000000000, -1.329743448921561232E-15 ) ) ;
#4721=ORIENTED_EDGE ( 'NONE', *, *, #6494, .F. ) ;
#4765=ORIENTED_EDGE ( 'NONE', *, *, #3182, .F. ) ;
#4769=DIRECTION ( 'NONE',  ( 0.000000000000000000, 0.000000000000000000, 1.000000000000000000 ) ) ;
#4775=VECTOR ( 'NONE', #9121, 999.9999999999998863 ) ;
#4781=ORIENTED_EDGE ( 'NONE', *, *, #7348, .F. ) ;
#4786=ORIENTED_EDGE ( 'NONE', *, *, #4447, .T. ) ;
#4798=AXIS2_PLACEMENT_3D ( 'NONE', #8526, #422, #5234 ) ;
#4832=FACE_OUTER_BOUND ( 'NONE', #10324, .T. ) ;
#4849=CARTESIAN_POINT ( 'NONE',  ( 3.000000000000000000, 2.935248768560057897, -3.252606517456513302E-15 ) ) ;
#4863=EDGE_CURVE ( 'NONE', #8078, #2498, #8394, .T. ) ;
#4864=CARTESIAN_POINT ( 'NONE',  ( 6.000000000000005329, 3.980102097228898231E-16, 3.250000000000000444 ) ) ;
#4890=CARTESIAN_POINT ( 'NONE',  ( 3.000000000000000000, 2.935248768560057897, -3.252606517456513302E-15 ) ) ;
#4893=CARTESIAN_POINT ( 'NONE',  ( 3.000000000000000000, 1.467624384280025174, -2.542000000000001592 ) ) ;
#4911=FACE_OUTER_BOUND ( 'NONE', #7740, .T. ) ;
#4921=DIRECTION ( 'NONE',  ( 0.000000000000000000, -1.000000000000000000, 1.329743448921561232E-15 ) ) ;
#4924=DIRECTION ( 'NONE',  ( 0.000000000000000000, 0.000000000000000000, 1.000000000000000000 ) ) ;
#4929=EDGE_CURVE ( 'NONE', #7226, #8168, #9145, .T. ) ;
#4942=EDGE_CURVE ( 'NONE', #910, #4373, #6530, .T. ) ;
#4946=ADVANCED_FACE ( 'NONE', ( #8614 ), #10211, .T. ) ;
#4964=DIRECTION ( 'NONE',  ( 0.000000000000000000, 0.000000000000000000, 1.000000000000000000 ) ) ;
#4982=ORIENTED_EDGE ( 'NONE', *, *, #8347, .T. ) ;
#4986=ORIENTED_EDGE ( 'NONE', *, *, #2751, .F. ) ;
#4987=FACE_OUTER_BOUND ( 'NONE', #9415, .T. ) ;
#4988=LINE ( 'NONE', #3302, #4086 ) ;
#5001=VERTEX_POINT ( 'NONE', #5481 ) ;
#5002=AXIS2_PLACEMENT_3D ( 'NONE', #4156, #9789, #1768 ) ;
#5009=DIRECTION ( 'NONE',  ( -1.000000000000000000, -0.000000000000000000, -0.000000000000000000 ) ) ;
#5016=AXIS2_PLACEMENT_3D ( 'NONE', #1203, #364, #3589 ) ;
#5051=ORIENTED_EDGE ( 'NONE', *, *, #678, .F. ) ;
#5054=ORIENTED_EDGE ( 'NONE', *, *, #428, .F. ) ;
#5068=SHAPE_REPRESENTATION ( 'socket head cap screw_iso_ISO 4762 M6 x 20 - 20N', ( #4601 ), #3113 ) ;
#5083=ORIENTED_EDGE ( 'NONE', *, *, #5478, .T. ) ;
#5108=EDGE_LOOP ( 'NONE', ( #6742, #5876, #5051, #1718, #3857 ) ) ;
#5122=AXIS2_PLACEMENT_3D ( 'NONE', #29, #5740, #5796 ) ;
#5129=DIRECTION ( 'NONE',  ( -1.000000000000000000, -0.000000000000000000, -0.000000000000000000 ) ) ;
#5131=DIRECTION ( 'NONE',  ( 0.000000000000000000, 0.000000000000000000, -1.000000000000000000 ) ) ;
#5132=DIRECTION ( 'NONE',  ( -1.000000000000000000, 0.000000000000000000, -0.000000000000000000 ) ) ;
#5142=EDGE_CURVE ( 'NONE', #910, #5311, #1966, .T. ) ;
#5155=DIRECTION ( 'NONE',  ( 0.000000000000000000, 0.000000000000000000, 1.000000000000000000 ) ) ;
#5159=CARTESIAN_POINT ( 'NONE',  ( 25.44550000000000978, 0.000000000000000000, 0.000000000000000000 ) ) ;
#5174=ORIENTED_EDGE ( 'NONE', *, *, #3992, .F. ) ;
#5186=AXIS2_PLACEMENT_3D ( 'NONE', #600, #4677, #3834 ) ;
#5188=AXIS2_PLACEMENT_3D ( 'NONE', #3476, #1244, #9198 ) ;
#5200=TOROIDAL_SURFACE ( 'NONE', #5701, 3.250000000000000444, 0.2500000000000000000 ) ;
#5218=EDGE_CURVE ( 'NONE', #2498, #8078, #4508, .T. ) ;
#5233=DIRECTION ( 'NONE',  ( 0.000000000000000000, 0.000000000000000000, 1.000000000000000000 ) ) ;
#5234=DIRECTION ( 'NONE',  ( 0.000000000000000000, 0.000000000000000000, 1.000000000000000000 ) ) ;
#5236=CIRCLE ( 'NONE', #5403, 4.700000000000000178 ) ;
#5268=VERTEX_POINT ( 'NONE', #2670 ) ;
#5278=EDGE_LOOP ( 'NONE', ( #2239, #4187, #5901, #3238, #9331 ) ) ;
#5287=CIRCLE ( 'NONE', #1229, 5.000000000000000000 ) ;
#5306=VECTOR ( 'NONE', #3376, 1000.000000000000114 ) ;
#5311=VERTEX_POINT ( 'NONE', #1238 ) ;
#5350=CARTESIAN_POINT ( 'NONE',  ( 3.000000000000000000, 2.935248768560057897, -3.252606517456513302E-15 ) ) ;
#5360=VECTOR ( 'NONE', #5861, 1000.000000000000000 ) ;
#5366=LINE ( 'NONE', #9625, #6458 ) ;
#5375=CARTESIAN_POINT ( 'NONE',  ( 3.000000000000000000, -2.935248768560057009, 4.770489558936219510E-15 ) ) ;
#5403=AXIS2_PLACEMENT_3D ( 'NONE', #5658, #106, #4964 ) ;
#5404=DIRECTION ( 'NONE',  ( -1.000000000000000000, -0.000000000000000000, -0.000000000000000000 ) ) ;
#5419=ORIENTED_EDGE ( 'NONE', *, *, #3182, .T. ) ;
#5434=ORIENTED_EDGE ( 'NONE', *, *, #3042, .T. ) ;
#5444=PLANE ( 'NONE',  #3986 ) ;
#5458=EDGE_CURVE ( 'NONE', #8005, #9088, #4625, .T. ) ;
#5478=EDGE_CURVE ( 'NONE', #9437, #1028, #853, .T. ) ;
#5481=CARTESIAN_POINT ( 'NONE',  ( 3.000000000000000000, -2.935248768560057009, 4.770489558936219510E-15 ) ) ;
#5486=EDGE_LOOP ( 'NONE', ( #8671, #2967, #5083, #4199, #1824 ) ) ;
#5505=( NAMED_UNIT ( * ) SI_UNIT ( $, .STERADIAN. ) SOLID_ANGLE_UNIT ( ) );
#5532=AXIS2_PLACEMENT_3D ( 'NONE', #5576, #5726, #4924 ) ;
#5540=VECTOR ( 'NONE', #6628, 1000.000000000000000 ) ;
#5564=EDGE_CURVE ( 'NONE', #8380, #477, #7225, .T. ) ;
#5565=ADVANCED_FACE ( 'NONE', ( #2347 ), #2499, .T. ) ;
#5576=CARTESIAN_POINT ( 'NONE',  ( -31.74999999999995737, 0.000000000000000000, 0.000000000000000000 ) ) ;
#5583=CARTESIAN_POINT ( 'NONE',  ( 0.000000000000000000, 1.467624384280033167, 2.541999999999999371 ) ) ;
#5623=ORIENTED_EDGE ( 'NONE', *, *, #6959, .T. ) ;
#5624=DIRECTION ( 'NONE',  ( 0.000000000000000000, 0.000000000000000000, 1.000000000000000000 ) ) ;
#5633=CARTESIAN_POINT ( 'NONE',  ( 3.000000000000000000, 3.380207847158609940E-15, 2.542000000000001592 ) ) ;
#5647=CARTESIAN_POINT ( 'NONE',  ( 3.000000000000000000, 1.467624384280032501, 2.541999999999999371 ) ) ;
#5658=CARTESIAN_POINT ( 'NONE',  ( 0.000000000000000000, 0.000000000000000000, 0.000000000000000000 ) ) ;
#5685=ORIENTED_EDGE ( 'NONE', *, *, #8347, .F. ) ;
#5700=ORIENTED_EDGE ( 'NONE', *, *, #9826, .F. ) ;
#5701=AXIS2_PLACEMENT_3D ( 'NONE', #10465, #4049, #2354 ) ;
#5726=DIRECTION ( 'NONE',  ( -1.000000000000000000, -0.000000000000000000, -0.000000000000000000 ) ) ;
#5740=DIRECTION ( 'NONE',  ( -1.000000000000000000, -0.000000000000000000, -0.000000000000000000 ) ) ;
#5770=STYLED_ITEM('',(#10525),#6821);
#5796=DIRECTION ( 'NONE',  ( 0.000000000000000000, 0.000000000000000000, 1.000000000000000000 ) ) ;
#5816=CARTESIAN_POINT ( 'NONE',  ( 0.000000000000000000, -2.935248768560057009, 4.770489558936219510E-15 ) ) ;
#5826=VECTOR ( 'NONE', #8717, 1000.000000000000114 ) ;
#5828=LINE ( 'NONE', #7478, #5540 ) ;
#5838=LINE ( 'NONE', #1072, #7303 ) ;
#5839=CARTESIAN_POINT ( 'NONE',  ( 3.000000000000000000, -3.380207847158608363E-15, -2.541999999999999815 ) ) ;
#5858=EDGE_CURVE ( 'NONE', #5268, #1613, #6731, .T. ) ;
#5861=DIRECTION ( 'NONE',  ( -1.000000000000000000, -0.000000000000000000, -0.000000000000000000 ) ) ;
#5865=LINE ( 'NONE', #4027, #6113 ) ;
#5876=ORIENTED_EDGE ( 'NONE', *, *, #3686, .F. ) ;
#5883=CARTESIAN_POINT ( 'NONE',  ( 3.000000000000000000, 1.467624384280025174, -2.542000000000001592 ) ) ;
#5899=CIRCLE ( 'NONE', #4552, 4.700000000000000178 ) ;
#5901=ORIENTED_EDGE ( 'NONE', *, *, #1440, .T. ) ;
#5905=EDGE_CURVE ( 'NONE', #2739, #10107, #5287, .T. ) ;
#5926=VERTEX_POINT ( 'NONE', #9910 ) ;
#5928=DIRECTION ( 'NONE',  ( 1.000000000000000000, 0.000000000000000000, 0.000000000000000000 ) ) ;
#5937=AXIS2_PLACEMENT_3D ( 'NONE', #5159, #9949, #1135 ) ;
#5943=FACE_OUTER_BOUND ( 'NONE', #5486, .T. ) ;
#5956=FACE_OUTER_BOUND ( 'NONE', #1364, .T. ) ;
#5983=DIRECTION ( 'NONE',  ( 0.000000000000000000, 0.000000000000000000, 1.000000000000000000 ) ) ;
#5989=PRODUCT_DEFINITION_FORMATION_WITH_SPECIFIED_SOURCE ( 'ANY', '', #8052, .NOT_KNOWN. ) ;
#5993=EDGE_CURVE ( 'NONE', #477, #5926, #7487, .T. ) ;
#6017=ORIENTED_EDGE ( 'NONE', *, *, #4516, .F. ) ;
#6018=AXIS2_PLACEMENT_3D ( 'NONE', #3954, #6333, #7184 ) ;
#6024=CARTESIAN_POINT ( 'NONE',  ( 3.000000000000000000, 1.467624384280025174, -2.542000000000001592 ) ) ;
#6043=VERTEX_POINT ( 'NONE', #10108 ) ;
#6048=ORIENTED_EDGE ( 'NONE', *, *, #1542, .F. ) ;
#6076=ORIENTED_EDGE ( 'NONE', *, *, #8687, .F. ) ;
#6082=DIRECTION ( 'NONE',  ( 1.000000000000000000, 0.000000000000000000, 0.000000000000000000 ) ) ;
#6113=VECTOR ( 'NONE', #4072, 1000.000000000000114 ) ;
#6134=FACE_OUTER_BOUND ( 'NONE', #8318, .T. ) ;
#6140=CARTESIAN_POINT ( 'NONE',  ( 0.000000000000000000, -1.467624384280024730, 2.542000000000003368 ) ) ;
#6148=DIRECTION ( 'NONE',  ( 0.000000000000000000, 0.8660254037844380415, -0.5000000000000012212 ) ) ;
#6156=AXIS2_PLACEMENT_3D ( 'NONE', #7455, #2633, #3424 ) ;
#6206=VERTEX_POINT ( 'NONE', #7931 ) ;
#6216=AXIS2_PLACEMENT_3D ( 'NONE', #7831, #9646, #10429 ) ;
#6233=LINE ( 'NONE', #3746, #1300 ) ;
#6241=CARTESIAN_POINT ( 'NONE',  ( 3.000000000000000000, 3.113052163432572109E-16, -2.541999999999999815 ) ) ;
#6258=APPLICATION_CONTEXT ( 'automotive_design' ) ;
#6274=CARTESIAN_POINT ( 'NONE',  ( 3.000000000000000000, 1.467624384280033167, 2.541999999999999371 ) ) ;
#6305=CARTESIAN_POINT ( 'NONE',  ( 3.000000000000000000, 1.467624384280025174, -2.542000000000001592 ) ) ;
#6322=PRODUCT_DEFINITION ( 'UNKNOWN', '', #5989, #182 ) ;
#6325=EDGE_CURVE ( 'NONE', #1057, #1613, #7499, .T. ) ;
#6333=DIRECTION ( 'NONE',  ( 0.000000000000000000, 1.000000000000000000, -1.224646799147353207E-16 ) ) ;
#6354=CARTESIAN_POINT ( 'NONE',  ( 3.000000000000000000, -2.201436576420041646, 1.271000000000002794 ) ) ;
#6366=EDGE_CURVE ( 'NONE', #1028, #9023, #395, .T. ) ;
#6367=DIRECTION ( 'NONE',  ( -1.000000000000000000, -0.000000000000000000, -0.000000000000000000 ) ) ;
#6414=VECTOR ( 'NONE', #10171, 1000.000000000000114 ) ;
#6441=DIRECTION ( 'NONE',  ( 0.000000000000000000, -0.8660254037844394848, -0.4999999999999985567 ) ) ;
#6458=VECTOR ( 'NONE', #10201, 1000.000000000000114 ) ;
#6470=EDGE_LOOP ( 'NONE', ( #9327, #7472, #5174, #4278, #8267 ) ) ;
#6486=CIRCLE ( 'NONE', #7507, 2.541999999999999815 ) ;
#6494=EDGE_CURVE ( 'NONE', #6206, #2621, #7836, .T. ) ;
#6499=DIRECTION ( 'NONE',  ( 0.000000000000000000, 0.000000000000000000, -1.000000000000000000 ) ) ;
#6502=DIRECTION ( 'NONE',  ( 1.000000000000000000, 0.000000000000000000, 0.000000000000000000 ) ) ;
#6511=DIRECTION ( 'NONE',  ( -1.000000000000000000, -0.000000000000000000, -0.000000000000000000 ) ) ;
#6522=DIRECTION ( 'NONE',  ( 0.000000000000000000, -1.000000000000000000, 1.329743448921561232E-15 ) ) ;
#6527=ORIENTED_EDGE ( 'NONE', *, *, #5858, .T. ) ;
#6530=CIRCLE ( 'NONE', #6018, 0.2500000000000002220 ) ;
#6560=PLANE ( 'NONE',  #958 ) ;
#6568=TOROIDAL_SURFACE ( 'NONE', #146, 4.700000000000000178, 0.2999999999999999889 ) ;
#6569=CARTESIAN_POINT ( 'NONE',  ( 0.000000000000000000, 0.000000000000000000, 0.000000000000000000 ) ) ;
#6619=AXIS2_PLACEMENT_3D ( 'NONE', #8195, #5009, #6660 ) ;
#6628=DIRECTION ( 'NONE',  ( -1.000000000000000000, -0.000000000000000000, -0.000000000000000000 ) ) ;
#6642=EDGE_CURVE ( 'NONE', #2621, #6206, #4591, .T. ) ;
#6660=DIRECTION ( 'NONE',  ( 0.000000000000000000, 0.000000000000000000, -1.000000000000000000 ) ) ;
#6700=EDGE_CURVE ( 'NONE', #9607, #3068, #5366, .T. ) ;
#6721=AXIS2_PLACEMENT_3D ( 'NONE', #7611, #2726, #9251 ) ;
#6724=FACE_OUTER_BOUND ( 'NONE', #5108, .T. ) ;
#6731=CIRCLE ( 'NONE', #9795, 2.541999999999999815 ) ;
#6734=DIRECTION ( 'NONE',  ( -1.000000000000000000, -0.000000000000000000, -0.000000000000000000 ) ) ;
#6740=CARTESIAN_POINT ( 'NONE',  ( 3.000000000000000000, -1.467624384280032279, -2.541999999999998039 ) ) ;
#6742=ORIENTED_EDGE ( 'NONE', *, *, #2032, .T. ) ;
#6743=CARTESIAN_POINT ( 'NONE',  ( 26.00000000000000355, 0.000000000000000000, 0.000000000000000000 ) ) ;
#6821=MANIFOLD_SOLID_BREP ( 'Hex', #1650 ) ;
#6825=ADVANCED_BREP_SHAPE_REPRESENTATION ( '', ( #6821, #4601 ), #3113 ) ;
#6826=AXIS2_PLACEMENT_3D ( 'NONE', #4293, #6734, #278 ) ;
#6935=CARTESIAN_POINT ( 'NONE',  ( 3.000000000000000000, 0.000000000000000000, 0.000000000000000000 ) ) ;
#6938=DIRECTION ( 'NONE',  ( 0.000000000000000000, -0.4999999999999985012, 0.8660254037844393737 ) ) ;
#6959=EDGE_CURVE ( 'NONE', #2709, #9023, #5865, .T. ) ;
#6979=PRODUCT_CONTEXT ( 'NONE', #7144, 'mechanical' ) ;
#7031=ADVANCED_FACE ( 'NONE', ( #7516 ), #2848, .T. ) ;
#7044=CARTESIAN_POINT ( 'NONE',  ( 0.000000000000000000, -1.467624384280032279, -2.541999999999998039 ) ) ;
#7047=CARTESIAN_POINT ( 'NONE',  ( 3.000000000000000000, 0.000000000000000000, 0.000000000000000000 ) ) ;
#7061=ORIENTED_EDGE ( 'NONE', *, *, #5993, .T. ) ;
#7081=EDGE_CURVE ( 'NONE', #9607, #1028, #9011, .T. ) ;
#7094=CARTESIAN_POINT ( 'NONE',  ( 3.000000000000000000, 2.935248768560057897, -3.252606517456513302E-15 ) ) ;
#7114=AXIS2_PLACEMENT_3D ( 'NONE', #4356, #7592, #4249 ) ;
#7120=VERTEX_POINT ( 'NONE', #1313 ) ;
#7127=ORIENTED_EDGE ( 'NONE', *, *, #3867, .T. ) ;
#7141=CARTESIAN_POINT ( 'NONE',  ( 26.00000000000000355, 3.334407072378455680E-16, -2.445500000000000007 ) ) ;
#7144=APPLICATION_CONTEXT ( 'automotive_design' ) ;
#7146=LINE ( 'NONE', #7094, #2133 ) ;
#7158=( LENGTH_UNIT ( ) NAMED_UNIT ( * ) SI_UNIT ( .MILLI., .METRE. ) );
#7160=CARTESIAN_POINT ( 'NONE',  ( -31.74999999999995737, 0.000000000000000000, 5.000000000000000000 ) ) ;
#7161=DIRECTION ( 'NONE',  ( 1.000000000000000000, 0.000000000000000000, 0.000000000000000000 ) ) ;
#7184=DIRECTION ( 'NONE',  ( 0.000000000000000000, 1.224646799147351482E-16, 1.000000000000000000 ) ) ;
#7197=AXIS2_PLACEMENT_3D ( 'NONE', #2433, #9866, #107 ) ;
#7214=AXIS2_PLACEMENT_3D ( 'NONE', #2210, #572, #624 ) ;
#7225=CIRCLE ( 'NONE', #2325, 5.000000000000000000 ) ;
#7226=VERTEX_POINT ( 'NONE', #519 ) ;
#7265=EDGE_LOOP ( 'NONE', ( #4236, #5623, #5434, #4982, #6527 ) ) ;
#7303=VECTOR ( 'NONE', #78, 1000.000000000000000 ) ;
#7314=ORIENTED_EDGE ( 'NONE', *, *, #2233, .F. ) ;
#7321=LINE ( 'NONE', #2495, #8685 ) ;
#7332=CARTESIAN_POINT ( 'NONE',  ( 3.000000000000000000, 1.467624384280032501, 2.541999999999999371 ) ) ;
#7348=EDGE_CURVE ( 'NONE', #3068, #8465, #8233, .T. ) ;
#7384=AXIS2_PLACEMENT_3D ( 'NONE', #2277, #6502, #2423 ) ;
#7385=DIRECTION ( 'NONE',  ( -1.000000000000000000, -0.000000000000000000, -0.000000000000000000 ) ) ;
#7394=VECTOR ( 'NONE', #3189, 1000.000000000000114 ) ;
#7425=ORIENTED_EDGE ( 'NONE', *, *, #4618, .T. ) ;
#7430=DIRECTION ( 'NONE',  ( 0.000000000000000000, -1.000000000000000000, 0.000000000000000000 ) ) ;
#7438=DIRECTION ( 'NONE',  ( -1.000000000000000000, -0.000000000000000000, -0.000000000000000000 ) ) ;
#7442=VECTOR ( 'NONE', #5129, 1000.000000000000000 ) ;
#7446=EDGE_LOOP ( 'NONE', ( #4786, #7127, #3726, #3421 ) ) ;
#7455=CARTESIAN_POINT ( 'NONE',  ( 0.3000000000000016542, 0.000000000000000000, 0.000000000000000000 ) ) ;
#7460=LINE ( 'NONE', #3484, #5360 ) ;
#7472=ORIENTED_EDGE ( 'NONE', *, *, #3313, .F. ) ;
#7478=CARTESIAN_POINT ( 'NONE',  ( -31.74999999999995737, 6.123233995736766282E-16, -5.000000000000000000 ) ) ;
#7487=CIRCLE ( 'NONE', #7657, 0.2999999999999999334 ) ;
#7499=LINE ( 'NONE', #4893, #1406 ) ;
#7506=DIRECTION ( 'NONE',  ( -1.000000000000000000, -0.000000000000000000, -0.000000000000000000 ) ) ;
#7507=AXIS2_PLACEMENT_3D ( 'NONE', #472, #1317, #5233 ) ;
#7516=FACE_OUTER_BOUND ( 'NONE', #7446, .T. ) ;
#7519=DIRECTION ( 'NONE',  ( 0.000000000000000000, 0.000000000000000000, 1.000000000000000000 ) ) ;
#7520=DIRECTION ( 'NONE',  ( -0.000000000000000000, 0.000000000000000000, 1.000000000000000000 ) ) ;
#7557=FACE_OUTER_BOUND ( 'NONE', #1498, .T. ) ;
#7592=DIRECTION ( 'NONE',  ( -0.000000000000000000, 1.000000000000000000, 1.224646799147353207E-16 ) ) ;
#7611=CARTESIAN_POINT ( 'NONE',  ( 0.3000000000000016542, 0.000000000000000000, 0.000000000000000000 ) ) ;
#7622=PLANE ( 'NONE',  #5016 ) ;
#7625=DIRECTION ( 'NONE',  ( -1.000000000000000000, -0.000000000000000000, -0.000000000000000000 ) ) ;
#7629=ADVANCED_FACE ( 'NONE', ( #3137 ), #2390, .T. ) ;
#7657=AXIS2_PLACEMENT_3D ( 'NONE', #9747, #8299, #6499 ) ;
#7674=EDGE_CURVE ( 'NONE', #8078, #2621, #3291, .T. ) ;
#7684=LINE ( 'NONE', #3817, #783 ) ;
#7690=PLANE ( 'NONE',  #9027 ) ;
#7702=CARTESIAN_POINT ( 'NONE',  ( 26.00000000000000355, 0.000000000000000000, 0.000000000000000000 ) ) ;
#7708=LINE ( 'NONE', #3632, #3512 ) ;
#7718=( NAMED_UNIT ( * ) PLANE_ANGLE_UNIT ( ) SI_UNIT ( $, .RADIAN. ) );
#7740=EDGE_LOOP ( 'NONE', ( #3344, #5419 ) ) ;
#7750=EDGE_CURVE ( 'NONE', #1613, #3068, #4087, .T. ) ;
#7791=ADVANCED_FACE ( 'NONE', ( #1061 ), #2589, .F. ) ;
#7815=EDGE_CURVE ( 'NONE', #7120, #8465, #7321, .T. ) ;
#7831=CARTESIAN_POINT ( 'NONE',  ( -31.74999999999995737, 0.000000000000000000, 0.000000000000000000 ) ) ;
#7836=CIRCLE ( 'NONE', #5937, 2.999999999999999556 ) ;
#7843=CARTESIAN_POINT ( 'NONE',  ( 3.000000000000000000, 1.467624384280025174, -2.542000000000001592 ) ) ;
#7905=DIRECTION ( 'NONE',  ( 0.000000000000000000, 0.000000000000000000, -1.000000000000000000 ) ) ;
#7922=CONICAL_SURFACE ( 'NONE', #3351, 2.445500000000000007, 0.7853981633974547183 ) ;
#7926=LINE ( 'NONE', #6274, #1480 ) ;
#7931=CARTESIAN_POINT ( 'NONE',  ( 25.44550000000000978, 3.673940397442059868E-16, -2.999999999999999556 ) ) ;
#7952=ORIENTED_EDGE ( 'NONE', *, *, #3992, .T. ) ;
#7968=ADVANCED_FACE ( 'NONE', ( #10079 ), #7690, .F. ) ;
#8005=VERTEX_POINT ( 'NONE', #2377 ) ;
#8010=CARTESIAN_POINT ( 'NONE',  ( 3.000000000000000000, 1.467624384280032501, 2.541999999999999371 ) ) ;
#8027=ORIENTED_EDGE ( 'NONE', *, *, #7674, .T. ) ;
#8032=AXIS2_PLACEMENT_3D ( 'NONE', #9759, #6511, #7519 ) ;
#8050=EDGE_CURVE ( 'NONE', #9059, #8005, #788, .T. ) ;
#8052=PRODUCT ( 'socket head cap screw_iso_ISO 4762 M6 x 20 - 20N', 'socket head cap screw_iso_ISO 4762 M6 x 20 - 20N', '', ( #6979 ) ) ;
#8060=EDGE_LOOP ( 'NONE', ( #9116, #7952, #1940 ) ) ;
#8078=VERTEX_POINT ( 'NONE', #588 ) ;
#8092=ORIENTED_EDGE ( 'NONE', *, *, #4942, .T. ) ;
#8107=ORIENTED_EDGE ( 'NONE', *, *, #3867, .F. ) ;
#8113=DIRECTION ( 'NONE',  ( -1.000000000000000000, -0.000000000000000000, -0.000000000000000000 ) ) ;
#8120=PLANE ( 'NONE',  #4701 ) ;
#8150=AXIS2_PLACEMENT_3D ( 'NONE', #10313, #4683, #8764 ) ;
#8168=VERTEX_POINT ( 'NONE', #3387 ) ;
#8189=DIRECTION ( 'NONE',  ( -1.000000000000000000, -0.000000000000000000, -0.000000000000000000 ) ) ;
#8195=CARTESIAN_POINT ( 'NONE',  ( 6.000000000000005329, 0.000000000000000000, 0.000000000000000000 ) ) ;
#8196=DIRECTION ( 'NONE',  ( -1.000000000000000000, -0.000000000000000000, -0.000000000000000000 ) ) ;
#8226=VECTOR ( 'NONE', #9719, 1000.000000000000114 ) ;
#8233=LINE ( 'NONE', #1820, #2253 ) ;
#8255=CARTESIAN_POINT ( 'NONE',  ( 3.000000000000000000, 1.467624384280032501, 2.541999999999999371 ) ) ;
#8267=ORIENTED_EDGE ( 'NONE', *, *, #8050, .T. ) ;
#8293=ORIENTED_EDGE ( 'NONE', *, *, #5218, .T. ) ;
#8299=DIRECTION ( 'NONE',  ( 0.000000000000000000, -1.000000000000000000, 0.000000000000000000 ) ) ;
#8318=EDGE_LOOP ( 'NONE', ( #622, #7314, #10175, #792, #3450 ) ) ;
#8334=DIRECTION ( 'NONE',  ( 0.000000000000000000, 0.000000000000000000, 1.000000000000000000 ) ) ;
#8347=EDGE_CURVE ( 'NONE', #10117, #5268, #6486, .T. ) ;
#8376=ADVANCED_FACE ( 'NONE', ( #6134 ), #3706, .T. ) ;
#8380=VERTEX_POINT ( 'NONE', #3599 ) ;
#8385=CARTESIAN_POINT ( 'NONE',  ( 6.000000000000005329, 0.000000000000000000, 0.000000000000000000 ) ) ;
#8388=DIRECTION ( 'NONE',  ( -1.000000000000000000, -0.000000000000000000, -0.000000000000000000 ) ) ;
#8394=CIRCLE ( 'NONE', #9408, 2.445500000000000007 ) ;
#8407=ORIENTED_EDGE ( 'NONE', *, *, #6325, .F. ) ;
#8465=VERTEX_POINT ( 'NONE', #7044 ) ;
#8526=CARTESIAN_POINT ( 'NONE',  ( 5.999999999999998224, 0.000000000000000000, 0.000000000000000000 ) ) ;
#8530=ORIENTED_EDGE ( 'NONE', *, *, #4516, .T. ) ;
#8586=CARTESIAN_POINT ( 'NONE',  ( 0.000000000000000000, 0.000000000000000000, 0.000000000000000000 ) ) ;
#8594=CIRCLE ( 'NONE', #1652, 0.2500000000000002220 ) ;
#8614=FACE_OUTER_BOUND ( 'NONE', #3961, .T. ) ;
#8621=ORIENTED_EDGE ( 'NONE', *, *, #7750, .T. ) ;
#8631=EDGE_LOOP ( 'NONE', ( #3123, #9146, #2140 ) ) ;
#8640=EDGE_CURVE ( 'NONE', #477, #8380, #2090, .T. ) ;
#8646=ORIENTED_EDGE ( 'NONE', *, *, #3081, .T. ) ;
#8665=ORIENTED_EDGE ( 'NONE', *, *, #8640, .F. ) ;
#8671=ORIENTED_EDGE ( 'NONE', *, *, #4929, .F. ) ;
#8685=VECTOR ( 'NONE', #4921, 1000.000000000000000 ) ;
#8687=EDGE_CURVE ( 'NONE', #10117, #6043, #1677, .T. ) ;
#8712=DIRECTION ( 'NONE',  ( 0.000000000000000000, -0.5000000000000012212, -0.8660254037844380415 ) ) ;
#8713=ADVANCED_FACE ( 'NONE', ( #828 ), #9044, .T. ) ;
#8717=DIRECTION ( 'NONE',  ( 0.000000000000000000, 0.4999999999999985567, -0.8660254037844394848 ) ) ;
#8732=CARTESIAN_POINT ( 'NONE',  ( 26.00000000000000355, 2.445500000000000007, 0.000000000000000000 ) ) ;
#8737=AXIS2_PLACEMENT_3D ( 'NONE', #1517, #2256, #8773 ) ;
#8764=DIRECTION ( 'NONE',  ( 0.000000000000000000, 0.000000000000000000, 1.000000000000000000 ) ) ;
#8769=CARTESIAN_POINT ( 'NONE',  ( 0.000000000000000000, 2.935248768560057897, -3.252606517456513302E-15 ) ) ;
#8773=DIRECTION ( 'NONE',  ( 0.000000000000000000, 0.000000000000000000, 1.000000000000000000 ) ) ;
#8838=FACE_BOUND ( 'NONE', #9008, .T. ) ;
#8851=ORIENTED_EDGE ( 'NONE', *, *, #7081, .F. ) ;
#8879=AXIS2_PLACEMENT_3D ( 'NONE', #1076, #6148, #9135 ) ;
#8882=EDGE_CURVE ( 'NONE', #5001, #9607, #2255, .T. ) ;
#9008=EDGE_LOOP ( 'NONE', ( #4409, #4667 ) ) ;
#9011=CIRCLE ( 'NONE', #214, 2.541999999999999815 ) ;
#9013=CARTESIAN_POINT ( 'NONE',  ( 3.000000000000000000, -1.467624384280024730, 2.542000000000003368 ) ) ;
#9023=VERTEX_POINT ( 'NONE', #5633 ) ;
#9025=FACE_OUTER_BOUND ( 'NONE', #8631, .T. ) ;
#9027=AXIS2_PLACEMENT_3D ( 'NONE', #6305, #9496, #4718 ) ;
#9034=AXIS2_PLACEMENT_3D ( 'NONE', #4495, #1895, #6938 ) ;
#9040=CARTESIAN_POINT ( 'NONE',  ( 4.467624384280048488, 0.000000000000000000, 0.000000000000000000 ) ) ;
#9044=PLANE ( 'NONE',  #1082 ) ;
#9057=VECTOR ( 'NONE', #3060, 1000.000000000000114 ) ;
#9059=VERTEX_POINT ( 'NONE', #4890 ) ;
#9086=ORIENTED_EDGE ( 'NONE', *, *, #5142, .T. ) ;
#9088=VERTEX_POINT ( 'NONE', #5583 ) ;
#9109=FACE_OUTER_BOUND ( 'NONE', #7265, .T. ) ;
#9116=ORIENTED_EDGE ( 'NONE', *, *, #5858, .F. ) ;
#9121=DIRECTION ( 'NONE',  ( -0.7071067811865431318, 0.000000000000000000, 0.7071067811865520136 ) ) ;
#9122=DIRECTION ( 'NONE',  ( 0.000000000000000000, 0.000000000000000000, -1.000000000000000000 ) ) ;
#9126=DIRECTION ( 'NONE',  ( 0.000000000000000000, 0.000000000000000000, 1.000000000000000000 ) ) ;
#9127=CIRCLE ( 'NONE', #3552, 2.541999999999999815 ) ;
#9129=ORIENTED_EDGE ( 'NONE', *, *, #10002, .F. ) ;
#9135=DIRECTION ( 'NONE',  ( 0.000000000000000000, 0.5000000000000011102, 0.8660254037844379305 ) ) ;
#9144=DIRECTION ( 'NONE',  ( 0.000000000000000000, 0.4999999999999985012, -0.8660254037844393737 ) ) ;
#9145=LINE ( 'NONE', #1885, #2308 ) ;
#9146=ORIENTED_EDGE ( 'NONE', *, *, #5478, .F. ) ;
#9147=DIRECTION ( 'NONE',  ( 0.000000000000000000, 0.000000000000000000, 1.000000000000000000 ) ) ;
#9166=ADVANCED_FACE ( 'NONE', ( #5943 ), #2668, .T. ) ;
#9197=ORIENTED_EDGE ( 'NONE', *, *, #6366, .T. ) ;
#9198=DIRECTION ( 'NONE',  ( 0.000000000000000000, 0.000000000000000000, 1.000000000000000000 ) ) ;
#9207=ORIENTED_EDGE ( 'NONE', *, *, #6642, .T. ) ;
#9210=ADVANCED_FACE ( 'NONE', ( #647 ), #9224, .F. ) ;
#9222=ORIENTED_EDGE ( 'NONE', *, *, #4942, .F. ) ;
#9224=TOROIDAL_SURFACE ( 'NONE', #3132, 3.250000000000000444, 0.2500000000000000000 ) ;
#9251=DIRECTION ( 'NONE',  ( 0.000000000000000000, 0.000000000000000000, 1.000000000000000000 ) ) ;
#9257=TOROIDAL_SURFACE ( 'NONE', #6721, 4.700000000000000178, 0.2999999999999999889 ) ;
#9282=DIRECTION ( 'NONE',  ( 0.000000000000000000, -0.5000000000000012212, -0.8660254037844380415 ) ) ;
#9308=PLANE ( 'NONE',  #5188 ) ;
#9322=LINE ( 'NONE', #6024, #7442 ) ;
#9327=ORIENTED_EDGE ( 'NONE', *, *, #105, .T. ) ;
#9331=ORIENTED_EDGE ( 'NONE', *, *, #3686, .T. ) ;
#9341=ORIENTED_EDGE ( 'NONE', *, *, #4863, .F. ) ;
#9342=ORIENTED_EDGE ( 'NONE', *, *, #5993, .F. ) ;
#9395=DIRECTION ( 'NONE',  ( -1.000000000000000000, -0.000000000000000000, -0.000000000000000000 ) ) ;
#9408=AXIS2_PLACEMENT_3D ( 'NONE', #1144, #7506, #2835 ) ;
#9415=EDGE_LOOP ( 'NONE', ( #2545, #3405, #1545, #1390 ) ) ;
#9418=AXIS2_PLACEMENT_3D ( 'NONE', #7702, #1924, #5155 ) ;
#9425=ADVANCED_FACE ( 'NONE', ( #6724 ), #1798, .F. ) ;
#9427=ADVANCED_FACE ( 'NONE', ( #4132, #4911 ), #4185, .T. ) ;
#9437=VERTEX_POINT ( 'NONE', #1050 ) ;
#9445=VECTOR ( 'NONE', #8712, 999.9999999999998863 ) ;
#9486=DIRECTION ( 'NONE',  ( 0.000000000000000000, 0.000000000000000000, 1.000000000000000000 ) ) ;
#9496=DIRECTION ( 'NONE',  ( 0.000000000000000000, -1.329743448921561232E-15, -1.000000000000000000 ) ) ;
#9504=PRODUCT_DEFINITION_SHAPE ( 'NONE', 'NONE',  #6322 ) ;
#9507=FACE_OUTER_BOUND ( 'NONE', #3495, .T. ) ;
#9511=DIRECTION ( 'NONE',  ( -1.000000000000000000, 0.000000000000000000, 0.000000000000000000 ) ) ;
#9607=VERTEX_POINT ( 'NONE', #3966 ) ;
#9623=CARTESIAN_POINT ( 'NONE',  ( 0.3000000000000016542, 0.000000000000000000, 0.000000000000000000 ) ) ;
#9625=CARTESIAN_POINT ( 'NONE',  ( 3.000000000000000000, -2.935248768560057009, 4.770489558936219510E-15 ) ) ;
#9646=DIRECTION ( 'NONE',  ( -1.000000000000000000, -0.000000000000000000, -0.000000000000000000 ) ) ;
#9676=ORIENTED_EDGE ( 'NONE', *, *, #8640, .T. ) ;
#9719=DIRECTION ( 'NONE',  ( 0.000000000000000000, -0.4999999999999985567, 0.8660254037844394848 ) ) ;
#9747=CARTESIAN_POINT ( 'NONE',  ( 0.3000000000000016542, 0.000000000000000000, 4.700000000000000178 ) ) ;
#9759=CARTESIAN_POINT ( 'NONE',  ( 3.000000000000000000, 0.000000000000000000, 0.000000000000000000 ) ) ;
#9768=ORIENTED_EDGE ( 'NONE', *, *, #1542, .T. ) ;
#9770=DIRECTION ( 'NONE',  ( 0.000000000000000000, 1.000000000000000000, -1.329743448921560837E-15 ) ) ;
#9776=DIRECTION ( 'NONE',  ( 1.000000000000000000, 0.000000000000000000, 0.000000000000000000 ) ) ;
#9789=DIRECTION ( 'NONE',  ( 1.000000000000000000, 0.000000000000000000, 0.000000000000000000 ) ) ;
#9795=AXIS2_PLACEMENT_3D ( 'NONE', #7047, #10285, #9486 ) ;
#9809=CARTESIAN_POINT ( 'NONE',  ( 3.000000000000000000, -1.467624384280024730, 2.542000000000003368 ) ) ;
#9826=EDGE_CURVE ( 'NONE', #4373, #3827, #1877, .T. ) ;
#9827=CARTESIAN_POINT ( 'NONE',  ( 0.000000000000000000, 2.935248768560057897, -3.252606517456513302E-15 ) ) ;
#9830=EDGE_LOOP ( 'NONE', ( #9207, #88, #8530, #6048 ) ) ;
#9843=EDGE_LOOP ( 'NONE', ( #1600, #8621, #328 ) ) ;
#9866=DIRECTION ( 'NONE',  ( -1.000000000000000000, -0.000000000000000000, -0.000000000000000000 ) ) ;
#9891=CARTESIAN_POINT ( 'NONE',  ( -31.74999999999995737, 0.000000000000000000, 3.000000000000000444 ) ) ;
#9910=CARTESIAN_POINT ( 'NONE',  ( 0.000000000000000000, 0.000000000000000000, 4.700000000000000178 ) ) ;
#9913=DIRECTION ( 'NONE',  ( -1.000000000000000000, 0.000000000000000000, 0.000000000000000000 ) ) ;
#9920=DIRECTION ( 'NONE',  ( 0.000000000000000000, -1.000000000000000000, 1.329743448921560837E-15 ) ) ;
#9923=ORIENTED_EDGE ( 'NONE', *, *, #678, .T. ) ;
#9929=CARTESIAN_POINT ( 'NONE',  ( 26.00000000000000355, 0.000000000000000000, 2.445500000000000007 ) ) ;
#9938=UNCERTAINTY_MEASURE_WITH_UNIT (LENGTH_MEASURE( 1.000000000000000082E-05 ), #411, 'distance_accuracy_value', 'NONE');
#9949=DIRECTION ( 'NONE',  ( -1.000000000000000000, -0.000000000000000000, -0.000000000000000000 ) ) ;
#9968=FACE_OUTER_BOUND ( 'NONE', #1693, .T. ) ;
#9977=EDGE_CURVE ( 'NONE', #9437, #9023, #5838, .T. ) ;
#9984=CARTESIAN_POINT ( 'NONE',  ( 6.000000000000005329, 0.000000000000000000, -3.250000000000000444 ) ) ;
#9990=ORIENTED_EDGE ( 'NONE', *, *, #3042, .F. ) ;
#10002=EDGE_CURVE ( 'NONE', #2498, #6206, #4988, .T. ) ;
#10012=FACE_OUTER_BOUND ( 'NONE', #8060, .T. ) ;
#10079=FACE_OUTER_BOUND ( 'NONE', #565, .T. ) ;
#10088=ORIENTED_EDGE ( 'NONE', *, *, #3979, .F. ) ;
#10107=VERTEX_POINT ( 'NONE', #4363 ) ;
#10108=CARTESIAN_POINT ( 'NONE',  ( 3.000000000000000000, 1.467624384280033167, 2.541999999999999371 ) ) ;
#10117=VERTEX_POINT ( 'NONE', #2926 ) ;
#10126=AXIS2_PLACEMENT_3D ( 'NONE', #8385, #9395, #543 ) ;
#10169=DIRECTION ( 'NONE',  ( -1.000000000000000000, -0.000000000000000000, -0.000000000000000000 ) ) ;
#10171=DIRECTION ( 'NONE',  ( 0.000000000000000000, 0.4999999999999985567, -0.8660254037844394848 ) ) ;
#10175=ORIENTED_EDGE ( 'NONE', *, *, #8882, .T. ) ;
#10201=DIRECTION ( 'NONE',  ( 0.000000000000000000, 0.4999999999999985567, -0.8660254037844394848 ) ) ;
#10211=CYLINDRICAL_SURFACE ( 'NONE', #8737, 3.000000000000000444 ) ;
#10228=CARTESIAN_POINT ( 'NONE',  ( 6.250000000000005329, 0.000000000000000000, 0.000000000000000000 ) ) ;
#10268=SHAPE_DEFINITION_REPRESENTATION ( #9504, #5068 ) ;
#10285=DIRECTION ( 'NONE',  ( -1.000000000000000000, -0.000000000000000000, -0.000000000000000000 ) ) ;
#10286=ORIENTED_EDGE ( 'NONE', *, *, #8882, .F. ) ;
#10313=CARTESIAN_POINT ( 'NONE',  ( 25.44550000000000978, 0.000000000000000000, 0.000000000000000000 ) ) ;
#10324=EDGE_LOOP ( 'NONE', ( #9222, #6017, #27, #5700 ) ) ;
#10347=CARTESIAN_POINT ( 'NONE',  ( 6.250000000000005329, 0.000000000000000000, 0.000000000000000000 ) ) ;
#10348=ORIENTED_EDGE ( 'NONE', *, *, #32, .F. ) ;
#10373=AXIS2_PLACEMENT_3D ( 'NONE', #8010, #9511, #2243 ) ;
#10380=LINE ( 'NONE', #6241, #9057 ) ;
#10399=ORIENTED_EDGE ( 'NONE', *, *, #5905, .F. ) ;
#10429=DIRECTION ( 'NONE',  ( 0.000000000000000000, 0.000000000000000000, 1.000000000000000000 ) ) ;
#10460=ORIENTED_EDGE ( 'NONE', *, *, #3081, .F. ) ;
#10465=CARTESIAN_POINT ( 'NONE',  ( 6.250000000000005329, 0.000000000000000000, 0.000000000000000000 ) ) ;
#10519=COLOUR_RGB('Black',0.12,0.14,0.17);
#10520=FILL_AREA_STYLE_COLOUR('',#10519);
#10521=FILL_AREA_STYLE('',(#10520));
#10522=SURFACE_STYLE_FILL_AREA(#10521);
#10523=SURFACE_SIDE_STYLE('',(#10522));
#10524=SURFACE_STYLE_USAGE(.BOTH.,#10523);
#10525=PRESENTATION_STYLE_ASSIGNMENT((#10524));
ENDSEC;
END-ISO-10303-21;
